ISO-10303-21;
HEADER;
/* Generated by software containing ST-Developer
 * from STEP Tools, Inc. (www.steptools.com) 
 */

FILE_DESCRIPTION(
/* description */ ('PAT-091'),
/* implementation_level */ '2;1');

FILE_NAME(
/* name */ 'M4 low-profile retaining screw (8).step',
/* time_stamp */ '2026-10-27T15:34:44-07:00',
/* author */ (''),
/* organization */ (''),
/* preprocessor_version */ 'ST-DEVELOPER v20.2',
/* originating_system */ 'Autodesk Translation Framework v15.17.0.0',
/* authorisation */ '');

FILE_SCHEMA (('AUTOMOTIVE_DESIGN { 1 0 10303 214 3 1 1 }'));
ENDSEC;

DATA;
#10=MECHANICAL_DESIGN_GEOMETRIC_PRESENTATION_REPRESENTATION('',(#1061),#25100);
#841=SHAPE_REPRESENTATION_RELATIONSHIP('SRR','None',#25608,#951);
#951=ADVANCED_BREP_SHAPE_REPRESENTATION('',(#1182),#25078);
#1061=STYLED_ITEM('',(#26198),#1182);
#1182=MANIFOLD_SOLID_BREP('Body1',#13341);
#1599=FACE_BOUND('',#3930,.T.);
#1998=PLANE('',#16032);
#1999=PLANE('',#16037);
#2000=PLANE('',#16040);
#2727=FACE_OUTER_BOUND('',#3929,.T.);
#2728=FACE_OUTER_BOUND('',#3931,.T.);
#2729=FACE_OUTER_BOUND('',#3932,.T.);
#2730=FACE_OUTER_BOUND('',#3933,.T.);
#2731=FACE_OUTER_BOUND('',#3934,.T.);
#3929=EDGE_LOOP('',(#11576));
#3930=EDGE_LOOP('',(#11577));
#3931=EDGE_LOOP('',(#11578,#11579,#11580,#11581));
#3932=EDGE_LOOP('',(#11582));
#3933=EDGE_LOOP('',(#11583,#11584,#11585,#11586));
#3934=EDGE_LOOP('',(#11587));
#4812=LINE('',#24036,#5552);
#4813=LINE('',#24042,#5553);
#5552=VECTOR('',#20058,0.350000000000001);
#5553=VECTOR('',#20067,0.199999999999999);
#6214=CIRCLE('',#16033,0.350000000000001);
#6215=CIRCLE('',#16034,0.199999999999999);
#6216=CIRCLE('',#16036,0.350000000000001);
#6217=CIRCLE('',#16039,0.199999999999999);
#7247=VERTEX_POINT('',#24030);
#7248=VERTEX_POINT('',#24032);
#7249=VERTEX_POINT('',#24035);
#7250=VERTEX_POINT('',#24040);
#8723=EDGE_CURVE('',#7247,#7247,#6214,.T.);
#8724=EDGE_CURVE('',#7248,#7248,#6215,.T.);
#8725=EDGE_CURVE('',#7247,#7249,#4812,.T.);
#8726=EDGE_CURVE('',#7249,#7249,#6216,.T.);
#8727=EDGE_CURVE('',#7250,#7250,#6217,.T.);
#8728=EDGE_CURVE('',#7250,#7248,#4813,.T.);
#11576=ORIENTED_EDGE('',*,*,#8723,.T.);
#11577=ORIENTED_EDGE('',*,*,#8724,.F.);
#11578=ORIENTED_EDGE('',*,*,#8723,.F.);
#11579=ORIENTED_EDGE('',*,*,#8725,.T.);
#11580=ORIENTED_EDGE('',*,*,#8726,.T.);
#11581=ORIENTED_EDGE('',*,*,#8725,.F.);
#11582=ORIENTED_EDGE('',*,*,#8726,.F.);
#11583=ORIENTED_EDGE('',*,*,#8727,.F.);
#11584=ORIENTED_EDGE('',*,*,#8728,.T.);
#11585=ORIENTED_EDGE('',*,*,#8724,.T.);
#11586=ORIENTED_EDGE('',*,*,#8728,.F.);
#11587=ORIENTED_EDGE('',*,*,#8727,.T.);
#12368=CYLINDRICAL_SURFACE('',#16035,0.350000000000001);
#12369=CYLINDRICAL_SURFACE('',#16038,0.199999999999999);
#13094=ADVANCED_FACE('',(#2727,#1599),#1998,.T.);
#13095=ADVANCED_FACE('',(#2728),#12368,.T.);
#13096=ADVANCED_FACE('',(#2729),#1999,.F.);
#13097=ADVANCED_FACE('',(#2730),#12369,.T.);
#13098=ADVANCED_FACE('',(#2731),#2000,.T.);
#13341=CLOSED_SHELL('',(#13094,#13095,#13096,#13097,#13098));
#16031=AXIS2_PLACEMENT_3D('',#24028,#20048,#20049);
#16032=AXIS2_PLACEMENT_3D('',#24029,#20050,#20051);
#16033=AXIS2_PLACEMENT_3D('',#24031,#20052,#20053);
#16034=AXIS2_PLACEMENT_3D('',#24033,#20054,#20055);
#16035=AXIS2_PLACEMENT_3D('',#24034,#20056,#20057);
#16036=AXIS2_PLACEMENT_3D('',#24037,#20059,#20060);
#16037=AXIS2_PLACEMENT_3D('',#24038,#20061,#20062);
#16038=AXIS2_PLACEMENT_3D('',#24039,#20063,#20064);
#16039=AXIS2_PLACEMENT_3D('',#24041,#20065,#20066);
#16040=AXIS2_PLACEMENT_3D('',#24043,#20068,#20069);
#20048=DIRECTION('axis',(0.,0.,1.));
#20049=DIRECTION('refdir',(1.,0.,0.));
#20050=DIRECTION('center_axis',(0.,1.,0.));
#20051=DIRECTION('ref_axis',(1.,0.,0.));
#20052=DIRECTION('center_axis',(0.,1.,0.));
#20053=DIRECTION('ref_axis',(1.,0.,0.));
#20054=DIRECTION('center_axis',(0.,1.,0.));
#20055=DIRECTION('ref_axis',(1.,0.,0.));
#20056=DIRECTION('center_axis',(0.,1.,0.));
#20057=DIRECTION('ref_axis',(1.,0.,0.));
#20058=DIRECTION('',(0.,-1.,0.));
#20059=DIRECTION('center_axis',(0.,1.,0.));
#20060=DIRECTION('ref_axis',(1.,0.,0.));
#20061=DIRECTION('center_axis',(0.,1.,0.));
#20062=DIRECTION('ref_axis',(1.,0.,0.));
#20063=DIRECTION('center_axis',(0.,1.,0.));
#20064=DIRECTION('ref_axis',(1.,0.,0.));
#20065=DIRECTION('center_axis',(0.,1.,0.));
#20066=DIRECTION('ref_axis',(1.,0.,0.));
#20067=DIRECTION('',(0.,-1.,0.));
#20068=DIRECTION('center_axis',(0.,1.,0.));
#20069=DIRECTION('ref_axis',(1.,0.,0.));
#24028=CARTESIAN_POINT('',(0.,0.,0.));
#24029=CARTESIAN_POINT('Origin',(20.6730642762322,6.7,9.30814754519511));
#24030=CARTESIAN_POINT('',(20.3230642762322,6.7,9.30814754519511));
#24031=CARTESIAN_POINT('Origin',(20.6730642762322,6.7,9.30814754519511));
#24032=CARTESIAN_POINT('',(20.4730642762322,6.7,9.30814754519511));
#24033=CARTESIAN_POINT('Origin',(20.6730642762322,6.7,9.30814754519511));
#24034=CARTESIAN_POINT('Origin',(20.6730642762322,6.6,9.30814754519511));
#24035=CARTESIAN_POINT('',(20.3230642762322,6.6,9.30814754519511));
#24036=CARTESIAN_POINT('',(20.3230642762322,6.6,9.30814754519511));
#24037=CARTESIAN_POINT('Origin',(20.6730642762322,6.6,9.30814754519511));
#24038=CARTESIAN_POINT('Origin',(20.6730642762322,6.6,9.30814754519511));
#24039=CARTESIAN_POINT('Origin',(20.6730642762322,6.7,9.30814754519511));
#24040=CARTESIAN_POINT('',(20.4730642762322,7.4,9.30814754519511));
#24041=CARTESIAN_POINT('Origin',(20.6730642762322,7.4,9.30814754519511));
#24042=CARTESIAN_POINT('',(20.4730642762322,6.7,9.30814754519511));
#24043=CARTESIAN_POINT('Origin',(20.6730642762322,7.4,9.30814754519511));
#24957=UNCERTAINTY_MEASURE_WITH_UNIT(LENGTH_MEASURE(0.001),#25101,
'DISTANCE_ACCURACY_VALUE',
'Maximum model space distance between geometric entities at asserted c
onnectivities');
#24979=UNCERTAINTY_MEASURE_WITH_UNIT(LENGTH_MEASURE(0.001),#25101,
'DISTANCE_ACCURACY_VALUE',
'Maximum model space distance between geometric entities at asserted c
onnectivities');
#25078=(
GEOMETRIC_REPRESENTATION_CONTEXT(3)
GLOBAL_UNCERTAINTY_ASSIGNED_CONTEXT((#24957))
GLOBAL_UNIT_ASSIGNED_CONTEXT((#25101,#25103,#25104))
REPRESENTATION_CONTEXT('','3D')
);
#25100=(
GEOMETRIC_REPRESENTATION_CONTEXT(3)
GLOBAL_UNCERTAINTY_ASSIGNED_CONTEXT((#24979))
GLOBAL_UNIT_ASSIGNED_CONTEXT((#25101,#25103,#25104))
REPRESENTATION_CONTEXT('','3D')
);
#25101=(
LENGTH_UNIT()
NAMED_UNIT(*)
SI_UNIT(.CENTI.,.METRE.)
);
#25103=(
NAMED_UNIT(*)
PLANE_ANGLE_UNIT()
SI_UNIT($,.RADIAN.)
);
#25104=(
NAMED_UNIT(*)
SI_UNIT($,.STERADIAN.)
SOLID_ANGLE_UNIT()
);
#25203=SHAPE_DEFINITION_REPRESENTATION(#25397,#25608);
#25397=PRODUCT_DEFINITION_SHAPE('',$,#25729);
#25608=SHAPE_REPRESENTATION('',(#16031),#25078);
#25630=PRODUCT_DEFINITION_CONTEXT('part definition',#25992,'design');
#25729=PRODUCT_DEFINITION('M4 low-profile retaining screw (8)',
'M4 low-profile retaining screw (8)',#25849,#25630);
#25849=PRODUCT_DEFINITION_FORMATION('',$,#26092);
#25992=APPLICATION_CONTEXT(
'Core Data for Automotive Mechanical Design Process');
#25993=PRODUCT_CONTEXT('part definition',#25992,'mechanical');
#26092=PRODUCT('M4 low-profile retaining screw (8)',
'M4 low-profile retaining screw (8)','M4 low-profile retaining screw (8)',(#25993));
#26192=COLOUR_RGB('Black',0.12,0.14,0.17);
#26193=FILL_AREA_STYLE_COLOUR('',#26192);
#26194=FILL_AREA_STYLE('',(#26193));
#26195=SURFACE_STYLE_FILL_AREA(#26194);
#26196=SURFACE_SIDE_STYLE('',(#26195));
#26197=SURFACE_STYLE_USAGE(.BOTH.,#26196);
#26198=PRESENTATION_STYLE_ASSIGNMENT((#26197));
ENDSEC;
END-ISO-10303-21;
